ISO-10303-21;
HEADER;
/* Generated by software containing ST-Developer
 * from STEP Tools, Inc. (www.steptools.com) 
 */

FILE_DESCRIPTION(
/* description */ ('Hand-crank flanged shaft unit'),
/* implementation_level */ '2;1');

FILE_NAME(
/* name */ 'Flange bolt sleeve (4).step',
/* time_stamp */ '2026-10-27T18:35:45-07:00',
/* author */ (''),
/* organization */ (''),
/* preprocessor_version */ 'ST-DEVELOPER v20.2',
/* originating_system */ 'Autodesk Translation Framework v15.17.0.0',
/* authorisation */ '');

FILE_SCHEMA (('AUTOMOTIVE_DESIGN { 1 0 10303 214 3 1 1 }'));
ENDSEC;

DATA;
#10=MECHANICAL_DESIGN_GEOMETRIC_PRESENTATION_REPRESENTATION('',(#284),#6805);
#244=SHAPE_REPRESENTATION_RELATIONSHIP('SRR','None',#6905,#264);
#264=ADVANCED_BREP_SHAPE_REPRESENTATION('',(#305),#6788);
#284=STYLED_ITEM('',(#7098),#305);
#305=MANIFOLD_SOLID_BREP('Body1',#3325);
#350=FACE_BOUND('',#778,.T.);
#351=FACE_BOUND('',#780,.T.);
#434=PLANE('',#3644);
#435=PLANE('',#3645);
#557=FACE_OUTER_BOUND('',#775,.T.);
#558=FACE_OUTER_BOUND('',#776,.T.);
#559=FACE_OUTER_BOUND('',#777,.T.);
#560=FACE_OUTER_BOUND('',#779,.T.);
#775=EDGE_LOOP('',(#2431,#2432,#2433,#2434));
#776=EDGE_LOOP('',(#2435,#2436,#2437,#2438));
#777=EDGE_LOOP('',(#2439));
#778=EDGE_LOOP('',(#2440));
#779=EDGE_LOOP('',(#2441));
#780=EDGE_LOOP('',(#2442));
#1035=LINE('',#5136,#1263);
#1036=LINE('',#5142,#1264);
#1263=VECTOR('',#4166,0.425);
#1264=VECTOR('',#4173,0.595);
#1473=CIRCLE('',#3639,0.425);
#1474=CIRCLE('',#3640,0.425);
#1475=CIRCLE('',#3642,0.595);
#1476=CIRCLE('',#3643,0.595);
#1629=VERTEX_POINT('',#5133);
#1630=VERTEX_POINT('',#5135);
#1631=VERTEX_POINT('',#5139);
#1632=VERTEX_POINT('',#5141);
#1933=EDGE_CURVE('',#1629,#1629,#1473,.T.);
#1934=EDGE_CURVE('',#1629,#1630,#1035,.T.);
#1935=EDGE_CURVE('',#1630,#1630,#1474,.T.);
#1936=EDGE_CURVE('',#1631,#1631,#1475,.T.);
#1937=EDGE_CURVE('',#1631,#1632,#1036,.T.);
#1938=EDGE_CURVE('',#1632,#1632,#1476,.T.);
#2431=ORIENTED_EDGE('',*,*,#1933,.F.);
#2432=ORIENTED_EDGE('',*,*,#1934,.T.);
#2433=ORIENTED_EDGE('',*,*,#1935,.T.);
#2434=ORIENTED_EDGE('',*,*,#1934,.F.);
#2435=ORIENTED_EDGE('',*,*,#1936,.F.);
#2436=ORIENTED_EDGE('',*,*,#1937,.T.);
#2437=ORIENTED_EDGE('',*,*,#1938,.T.);
#2438=ORIENTED_EDGE('',*,*,#1937,.F.);
#2439=ORIENTED_EDGE('',*,*,#1936,.T.);
#2440=ORIENTED_EDGE('',*,*,#1933,.T.);
#2441=ORIENTED_EDGE('',*,*,#1938,.F.);
#2442=ORIENTED_EDGE('',*,*,#1935,.F.);
#3085=CYLINDRICAL_SURFACE('',#3638,0.425);
#3086=CYLINDRICAL_SURFACE('',#3641,0.595);
#3174=ADVANCED_FACE('',(#557),#3085,.F.);
#3175=ADVANCED_FACE('',(#558),#3086,.T.);
#3176=ADVANCED_FACE('',(#559,#350),#434,.T.);
#3177=ADVANCED_FACE('',(#560,#351),#435,.F.);
#3325=CLOSED_SHELL('',(#3174,#3175,#3176,#3177));
#3637=AXIS2_PLACEMENT_3D('',#5131,#4160,#4161);
#3638=AXIS2_PLACEMENT_3D('',#5132,#4162,#4163);
#3639=AXIS2_PLACEMENT_3D('',#5134,#4164,#4165);
#3640=AXIS2_PLACEMENT_3D('',#5137,#4167,#4168);
#3641=AXIS2_PLACEMENT_3D('',#5138,#4169,#4170);
#3642=AXIS2_PLACEMENT_3D('',#5140,#4171,#4172);
#3643=AXIS2_PLACEMENT_3D('',#5143,#4174,#4175);
#3644=AXIS2_PLACEMENT_3D('',#5144,#4176,#4177);
#3645=AXIS2_PLACEMENT_3D('',#5145,#4178,#4179);
#4160=DIRECTION('axis',(0.,0.,1.));
#4161=DIRECTION('refdir',(1.,0.,0.));
#4162=DIRECTION('center_axis',(0.,1.,0.));
#4163=DIRECTION('ref_axis',(1.,0.,0.));
#4164=DIRECTION('center_axis',(0.,-1.,0.));
#4165=DIRECTION('ref_axis',(1.,0.,0.));
#4166=DIRECTION('',(0.,-1.,0.));
#4167=DIRECTION('center_axis',(0.,-1.,0.));
#4168=DIRECTION('ref_axis',(1.,0.,0.));
#4169=DIRECTION('center_axis',(0.,1.,0.));
#4170=DIRECTION('ref_axis',(1.,0.,0.));
#4171=DIRECTION('center_axis',(0.,1.,0.));
#4172=DIRECTION('ref_axis',(1.,0.,0.));
#4173=DIRECTION('',(0.,-1.,0.));
#4174=DIRECTION('center_axis',(0.,1.,0.));
#4175=DIRECTION('ref_axis',(1.,0.,0.));
#4176=DIRECTION('center_axis',(0.,1.,0.));
#4177=DIRECTION('ref_axis',(1.,0.,0.));
#4178=DIRECTION('center_axis',(0.,1.,0.));
#4179=DIRECTION('ref_axis',(1.,0.,0.));
#5131=CARTESIAN_POINT('',(0.,0.,0.));
#5132=CARTESIAN_POINT('Origin',(-3.2,21.,4.3));
#5133=CARTESIAN_POINT('',(-3.625,22.,4.3));
#5134=CARTESIAN_POINT('Origin',(-3.2,22.,4.3));
#5135=CARTESIAN_POINT('',(-3.625,21.,4.3));
#5136=CARTESIAN_POINT('',(-3.625,21.,4.3));
#5137=CARTESIAN_POINT('Origin',(-3.2,21.,4.3));
#5138=CARTESIAN_POINT('Origin',(-3.2,21.,4.3));
#5139=CARTESIAN_POINT('',(-3.795,22.,4.3));
#5140=CARTESIAN_POINT('Origin',(-3.2,22.,4.3));
#5141=CARTESIAN_POINT('',(-3.795,21.,4.3));
#5142=CARTESIAN_POINT('',(-3.795,21.,4.3));
#5143=CARTESIAN_POINT('Origin',(-3.2,21.,4.3));
#5144=CARTESIAN_POINT('Origin',(-3.2,22.,4.3));
#5145=CARTESIAN_POINT('Origin',(-3.2,21.,4.3));
#6763=UNCERTAINTY_MEASURE_WITH_UNIT(LENGTH_MEASURE(0.001),#6806,
'DISTANCE_ACCURACY_VALUE',
'Maximum model space distance between geometric entities at asserted c
onnectivities');
#6780=UNCERTAINTY_MEASURE_WITH_UNIT(LENGTH_MEASURE(0.001),#6806,
'DISTANCE_ACCURACY_VALUE',
'Maximum model space distance between geometric entities at asserted c
onnectivities');
#6788=(
GEOMETRIC_REPRESENTATION_CONTEXT(3)
GLOBAL_UNCERTAINTY_ASSIGNED_CONTEXT((#6763))
GLOBAL_UNIT_ASSIGNED_CONTEXT((#6806,#6808,#6809))
REPRESENTATION_CONTEXT('','3D')
);
#6805=(
GEOMETRIC_REPRESENTATION_CONTEXT(3)
GLOBAL_UNCERTAINTY_ASSIGNED_CONTEXT((#6780))
GLOBAL_UNIT_ASSIGNED_CONTEXT((#6806,#6808,#6809))
REPRESENTATION_CONTEXT('','3D')
);
#6806=(
LENGTH_UNIT()
NAMED_UNIT(*)
SI_UNIT(.CENTI.,.METRE.)
);
#6808=(
NAMED_UNIT(*)
PLANE_ANGLE_UNIT()
SI_UNIT($,.RADIAN.)
);
#6809=(
NAMED_UNIT(*)
SI_UNIT($,.STERADIAN.)
SOLID_ANGLE_UNIT()
);
#6817=SHAPE_DEFINITION_REPRESENTATION(#6841,#6905);
#6841=PRODUCT_DEFINITION_SHAPE('',$,#6930);
#6905=SHAPE_REPRESENTATION('',(#3637),#6788);
#6922=PRODUCT_DEFINITION_CONTEXT('part definition',#6996,'design');
#6930=PRODUCT_DEFINITION('Flange bolt sleeve (4)',
'Flange bolt sleeve (4)',#6954,#6922);
#6954=PRODUCT_DEFINITION_FORMATION('',$,#7005);
#6996=APPLICATION_CONTEXT(
'Core Data for Automotive Mechanical Design Process');
#6997=PRODUCT_CONTEXT('part definition',#6996,'mechanical');
#7005=PRODUCT('Flange bolt sleeve (4)','Flange bolt sleeve (4)',
'Flange bolt sleeve (4)',(#6997));
#7092=COLOUR_RGB('Black',0.12,0.14,0.17);
#7093=FILL_AREA_STYLE_COLOUR('',#7092);
#7094=FILL_AREA_STYLE('',(#7093));
#7095=SURFACE_STYLE_FILL_AREA(#7094);
#7096=SURFACE_SIDE_STYLE('',(#7095));
#7097=SURFACE_STYLE_USAGE(.BOTH.,#7096);
#7098=PRESENTATION_STYLE_ASSIGNMENT((#7097));
ENDSEC;
END-ISO-10303-21;
